ISO-10303-21;
HEADER;
/* Generated by software containing ST-Developer
 * from STEP Tools, Inc. (www.steptools.com) 
 */

FILE_DESCRIPTION(
/* description */ ('Spring compression tester'),
/* implementation_level */ '2;1');

FILE_NAME(
/* name */ 'M5x8 ruler screw.step',
/* time_stamp */ '2026-10-28T03:24:11-07:00',
/* author */ (''),
/* organization */ (''),
/* preprocessor_version */ 'ST-DEVELOPER v20.2',
/* originating_system */ 'Autodesk Translation Framework v15.17.0.0',
/* authorisation */ '');

FILE_SCHEMA (('AUTOMOTIVE_DESIGN { 1 0 10303 214 3 1 1 }'));
ENDSEC;

DATA;
#10=MECHANICAL_DESIGN_GEOMETRIC_PRESENTATION_REPRESENTATION('',(#1157),#43521);
#968=CONICAL_SURFACE('',#20408,0.4,0.785398163397448);
#969=CONICAL_SURFACE('',#20412,0.41,0.785398163397448);
#970=CONICAL_SURFACE('',#20416,0.26,0.463647609000806);
#1022=SHAPE_REPRESENTATION_RELATIONSHIP('SRR','None',#43836,#1082);
#1082=ADVANCED_BREP_SHAPE_REPRESENTATION('',(#1228),#43496);
#1157=STYLED_ITEM('',(#44209),#1228);
#1228=MANIFOLD_SOLID_BREP('Body1',#18598);
#1475=FACE_BOUND('',#4083,.T.);
#1476=FACE_BOUND('',#4089,.T.);
#2014=PLANE('',#20404);
#2015=PLANE('',#20406);
#2016=PLANE('',#20414);
#2017=PLANE('',#20419);
#2018=PLANE('',#20420);
#2019=PLANE('',#20421);
#2020=PLANE('',#20422);
#2021=PLANE('',#20423);
#2022=PLANE('',#20424);
#2023=PLANE('',#20425);
#2807=FACE_OUTER_BOUND('',#4082,.T.);
#2808=FACE_OUTER_BOUND('',#4084,.T.);
#2809=FACE_OUTER_BOUND('',#4085,.T.);
#2810=FACE_OUTER_BOUND('',#4086,.T.);
#2811=FACE_OUTER_BOUND('',#4087,.T.);
#2812=FACE_OUTER_BOUND('',#4088,.T.);
#2813=FACE_OUTER_BOUND('',#4090,.T.);
#2814=FACE_OUTER_BOUND('',#4091,.T.);
#2815=FACE_OUTER_BOUND('',#4092,.T.);
#2816=FACE_OUTER_BOUND('',#4093,.T.);
#2817=FACE_OUTER_BOUND('',#4094,.T.);
#2818=FACE_OUTER_BOUND('',#4095,.T.);
#2819=FACE_OUTER_BOUND('',#4096,.T.);
#2820=FACE_OUTER_BOUND('',#4097,.T.);
#2821=FACE_OUTER_BOUND('',#4098,.T.);
#4082=EDGE_LOOP('',(#15069));
#4083=EDGE_LOOP('',(#15070,#15071,#15072,#15073,#15074,#15075));
#4084=EDGE_LOOP('',(#15076));
#4085=EDGE_LOOP('',(#15077,#15078,#15079,#15080));
#4086=EDGE_LOOP('',(#15081,#15082,#15083,#15084));
#4087=EDGE_LOOP('',(#15085,#15086,#15087,#15088));
#4088=EDGE_LOOP('',(#15089));
#4089=EDGE_LOOP('',(#15090));
#4090=EDGE_LOOP('',(#15091,#15092,#15093,#15094));
#4091=EDGE_LOOP('',(#15095,#15096,#15097,#15098));
#4092=EDGE_LOOP('',(#15099,#15100,#15101,#15102));
#4093=EDGE_LOOP('',(#15103,#15104,#15105,#15106));
#4094=EDGE_LOOP('',(#15107,#15108,#15109,#15110));
#4095=EDGE_LOOP('',(#15111,#15112,#15113,#15114));
#4096=EDGE_LOOP('',(#15115,#15116,#15117,#15118));
#4097=EDGE_LOOP('',(#15119,#15120,#15121,#15122));
#4098=EDGE_LOOP('',(#15123,#15124,#15125,#15126,#15127,#15128));
#5570=LINE('',#30168,#7002);
#5571=LINE('',#30170,#7003);
#5572=LINE('',#30172,#7004);
#5573=LINE('',#30174,#7005);
#5574=LINE('',#30176,#7006);
#5575=LINE('',#30177,#7007);
#5576=LINE('',#30184,#7008);
#5577=LINE('',#30188,#7009);
#5578=LINE('',#30192,#7010);
#5579=LINE('',#30199,#7011);
#5580=LINE('',#30201,#7012);
#5581=LINE('',#30205,#7013);
#5582=LINE('',#30206,#7014);
#5583=LINE('',#30207,#7015);
#5584=LINE('',#30210,#7016);
#5585=LINE('',#30211,#7017);
#5586=LINE('',#30214,#7018);
#5587=LINE('',#30215,#7019);
#5588=LINE('',#30218,#7020);
#5589=LINE('',#30219,#7021);
#5590=LINE('',#30222,#7022);
#5591=LINE('',#30223,#7023);
#5592=LINE('',#30225,#7024);
#7002=VECTOR('',#24404,1.);
#7003=VECTOR('',#24405,1.);
#7004=VECTOR('',#24406,1.);
#7005=VECTOR('',#24407,1.);
#7006=VECTOR('',#24408,1.);
#7007=VECTOR('',#24409,1.);
#7008=VECTOR('',#24418,0.4);
#7009=VECTOR('',#24423,0.425);
#7010=VECTOR('',#24428,0.41);
#7011=VECTOR('',#24437,0.26);
#7012=VECTOR('',#24440,0.25);
#7013=VECTOR('',#24443,1.);
#7014=VECTOR('',#24444,1.);
#7015=VECTOR('',#24445,1.);
#7016=VECTOR('',#24448,1.);
#7017=VECTOR('',#24449,1.);
#7018=VECTOR('',#24452,1.);
#7019=VECTOR('',#24453,1.);
#7020=VECTOR('',#24456,1.);
#7021=VECTOR('',#24457,1.);
#7022=VECTOR('',#24460,1.);
#7023=VECTOR('',#24461,1.);
#7024=VECTOR('',#24464,1.);
#7898=CIRCLE('',#20405,0.24505);
#7899=CIRCLE('',#20407,0.375);
#7900=CIRCLE('',#20409,0.425);
#7901=CIRCLE('',#20411,0.425);
#7902=CIRCLE('',#20413,0.395);
#7903=CIRCLE('',#20415,0.27);
#7904=CIRCLE('',#20417,0.24505);
#9099=VERTEX_POINT('',#30164);
#9100=VERTEX_POINT('',#30166);
#9101=VERTEX_POINT('',#30167);
#9102=VERTEX_POINT('',#30169);
#9103=VERTEX_POINT('',#30171);
#9104=VERTEX_POINT('',#30173);
#9105=VERTEX_POINT('',#30175);
#9106=VERTEX_POINT('',#30179);
#9107=VERTEX_POINT('',#30182);
#9108=VERTEX_POINT('',#30186);
#9109=VERTEX_POINT('',#30190);
#9110=VERTEX_POINT('',#30194);
#9111=VERTEX_POINT('',#30197);
#9112=VERTEX_POINT('',#30203);
#9113=VERTEX_POINT('',#30204);
#9114=VERTEX_POINT('',#30209);
#9115=VERTEX_POINT('',#30213);
#9116=VERTEX_POINT('',#30217);
#9117=VERTEX_POINT('',#30221);
#11199=EDGE_CURVE('',#9099,#9099,#7898,.T.);
#11200=EDGE_CURVE('',#9100,#9101,#5570,.T.);
#11201=EDGE_CURVE('',#9102,#9100,#5571,.T.);
#11202=EDGE_CURVE('',#9103,#9102,#5572,.T.);
#11203=EDGE_CURVE('',#9104,#9103,#5573,.T.);
#11204=EDGE_CURVE('',#9105,#9104,#5574,.T.);
#11205=EDGE_CURVE('',#9101,#9105,#5575,.T.);
#11206=EDGE_CURVE('',#9106,#9106,#7899,.T.);
#11207=EDGE_CURVE('',#9107,#9107,#7900,.T.);
#11208=EDGE_CURVE('',#9107,#9106,#5576,.T.);
#11209=EDGE_CURVE('',#9108,#9108,#7901,.T.);
#11210=EDGE_CURVE('',#9108,#9107,#5577,.T.);
#11211=EDGE_CURVE('',#9109,#9109,#7902,.T.);
#11212=EDGE_CURVE('',#9109,#9108,#5578,.T.);
#11213=EDGE_CURVE('',#9110,#9110,#7903,.T.);
#11214=EDGE_CURVE('',#9111,#9111,#7904,.F.);
#11215=EDGE_CURVE('',#9111,#9110,#5579,.T.);
#11216=EDGE_CURVE('',#9099,#9111,#5580,.T.);
#11217=EDGE_CURVE('',#9112,#9113,#5581,.T.);
#11218=EDGE_CURVE('',#9113,#9100,#5582,.T.);
#11219=EDGE_CURVE('',#9112,#9101,#5583,.T.);
#11220=EDGE_CURVE('',#9113,#9114,#5584,.T.);
#11221=EDGE_CURVE('',#9114,#9102,#5585,.T.);
#11222=EDGE_CURVE('',#9114,#9115,#5586,.T.);
#11223=EDGE_CURVE('',#9115,#9103,#5587,.T.);
#11224=EDGE_CURVE('',#9115,#9116,#5588,.T.);
#11225=EDGE_CURVE('',#9116,#9104,#5589,.T.);
#11226=EDGE_CURVE('',#9116,#9117,#5590,.T.);
#11227=EDGE_CURVE('',#9117,#9105,#5591,.T.);
#11228=EDGE_CURVE('',#9117,#9112,#5592,.T.);
#15069=ORIENTED_EDGE('',*,*,#11199,.F.);
#15070=ORIENTED_EDGE('',*,*,#11200,.F.);
#15071=ORIENTED_EDGE('',*,*,#11201,.F.);
#15072=ORIENTED_EDGE('',*,*,#11202,.F.);
#15073=ORIENTED_EDGE('',*,*,#11203,.F.);
#15074=ORIENTED_EDGE('',*,*,#11204,.F.);
#15075=ORIENTED_EDGE('',*,*,#11205,.F.);
#15076=ORIENTED_EDGE('',*,*,#11206,.F.);
#15077=ORIENTED_EDGE('',*,*,#11207,.F.);
#15078=ORIENTED_EDGE('',*,*,#11208,.T.);
#15079=ORIENTED_EDGE('',*,*,#11206,.T.);
#15080=ORIENTED_EDGE('',*,*,#11208,.F.);
#15081=ORIENTED_EDGE('',*,*,#11209,.F.);
#15082=ORIENTED_EDGE('',*,*,#11210,.T.);
#15083=ORIENTED_EDGE('',*,*,#11207,.T.);
#15084=ORIENTED_EDGE('',*,*,#11210,.F.);
#15085=ORIENTED_EDGE('',*,*,#11211,.F.);
#15086=ORIENTED_EDGE('',*,*,#11212,.T.);
#15087=ORIENTED_EDGE('',*,*,#11209,.T.);
#15088=ORIENTED_EDGE('',*,*,#11212,.F.);
#15089=ORIENTED_EDGE('',*,*,#11211,.T.);
#15090=ORIENTED_EDGE('',*,*,#11213,.F.);
#15091=ORIENTED_EDGE('',*,*,#11214,.F.);
#15092=ORIENTED_EDGE('',*,*,#11215,.T.);
#15093=ORIENTED_EDGE('',*,*,#11213,.T.);
#15094=ORIENTED_EDGE('',*,*,#11215,.F.);
#15095=ORIENTED_EDGE('',*,*,#11199,.T.);
#15096=ORIENTED_EDGE('',*,*,#11216,.T.);
#15097=ORIENTED_EDGE('',*,*,#11214,.T.);
#15098=ORIENTED_EDGE('',*,*,#11216,.F.);
#15099=ORIENTED_EDGE('',*,*,#11217,.T.);
#15100=ORIENTED_EDGE('',*,*,#11218,.T.);
#15101=ORIENTED_EDGE('',*,*,#11200,.T.);
#15102=ORIENTED_EDGE('',*,*,#11219,.F.);
#15103=ORIENTED_EDGE('',*,*,#11220,.T.);
#15104=ORIENTED_EDGE('',*,*,#11221,.T.);
#15105=ORIENTED_EDGE('',*,*,#11201,.T.);
#15106=ORIENTED_EDGE('',*,*,#11218,.F.);
#15107=ORIENTED_EDGE('',*,*,#11222,.T.);
#15108=ORIENTED_EDGE('',*,*,#11223,.T.);
#15109=ORIENTED_EDGE('',*,*,#11202,.T.);
#15110=ORIENTED_EDGE('',*,*,#11221,.F.);
#15111=ORIENTED_EDGE('',*,*,#11224,.T.);
#15112=ORIENTED_EDGE('',*,*,#11225,.T.);
#15113=ORIENTED_EDGE('',*,*,#11203,.T.);
#15114=ORIENTED_EDGE('',*,*,#11223,.F.);
#15115=ORIENTED_EDGE('',*,*,#11226,.T.);
#15116=ORIENTED_EDGE('',*,*,#11227,.T.);
#15117=ORIENTED_EDGE('',*,*,#11204,.T.);
#15118=ORIENTED_EDGE('',*,*,#11225,.F.);
#15119=ORIENTED_EDGE('',*,*,#11228,.T.);
#15120=ORIENTED_EDGE('',*,*,#11219,.T.);
#15121=ORIENTED_EDGE('',*,*,#11205,.T.);
#15122=ORIENTED_EDGE('',*,*,#11227,.F.);
#15123=ORIENTED_EDGE('',*,*,#11228,.F.);
#15124=ORIENTED_EDGE('',*,*,#11226,.F.);
#15125=ORIENTED_EDGE('',*,*,#11224,.F.);
#15126=ORIENTED_EDGE('',*,*,#11222,.F.);
#15127=ORIENTED_EDGE('',*,*,#11220,.F.);
#15128=ORIENTED_EDGE('',*,*,#11217,.F.);
#17260=CYLINDRICAL_SURFACE('',#20410,0.425);
#17261=CYLINDRICAL_SURFACE('',#20418,0.24505);
#18131=ADVANCED_FACE('',(#2807,#1475),#2014,.F.);
#18132=ADVANCED_FACE('',(#2808),#2015,.T.);
#18133=ADVANCED_FACE('',(#2809),#968,.T.);
#18134=ADVANCED_FACE('',(#2810),#17260,.T.);
#18135=ADVANCED_FACE('',(#2811),#969,.T.);
#18136=ADVANCED_FACE('',(#2812,#1476),#2016,.T.);
#18137=ADVANCED_FACE('',(#2813),#970,.T.);
#18138=ADVANCED_FACE('',(#2814),#17261,.T.);
#18139=ADVANCED_FACE('',(#2815),#2017,.F.);
#18140=ADVANCED_FACE('',(#2816),#2018,.F.);
#18141=ADVANCED_FACE('',(#2817),#2019,.F.);
#18142=ADVANCED_FACE('',(#2818),#2020,.F.);
#18143=ADVANCED_FACE('',(#2819),#2021,.F.);
#18144=ADVANCED_FACE('',(#2820),#2022,.F.);
#18145=ADVANCED_FACE('',(#2821),#2023,.F.);
#18598=CLOSED_SHELL('',(#18131,#18132,#18133,#18134,#18135,#18136,#18137,
#18138,#18139,#18140,#18141,#18142,#18143,#18144,#18145));
#20403=AXIS2_PLACEMENT_3D('',#30162,#24398,#24399);
#20404=AXIS2_PLACEMENT_3D('',#30163,#24400,#24401);
#20405=AXIS2_PLACEMENT_3D('',#30165,#24402,#24403);
#20406=AXIS2_PLACEMENT_3D('',#30178,#24410,#24411);
#20407=AXIS2_PLACEMENT_3D('',#30180,#24412,#24413);
#20408=AXIS2_PLACEMENT_3D('',#30181,#24414,#24415);
#20409=AXIS2_PLACEMENT_3D('',#30183,#24416,#24417);
#20410=AXIS2_PLACEMENT_3D('',#30185,#24419,#24420);
#20411=AXIS2_PLACEMENT_3D('',#30187,#24421,#24422);
#20412=AXIS2_PLACEMENT_3D('',#30189,#24424,#24425);
#20413=AXIS2_PLACEMENT_3D('',#30191,#24426,#24427);
#20414=AXIS2_PLACEMENT_3D('',#30193,#24429,#24430);
#20415=AXIS2_PLACEMENT_3D('',#30195,#24431,#24432);
#20416=AXIS2_PLACEMENT_3D('',#30196,#24433,#24434);
#20417=AXIS2_PLACEMENT_3D('',#30198,#24435,#24436);
#20418=AXIS2_PLACEMENT_3D('',#30200,#24438,#24439);
#20419=AXIS2_PLACEMENT_3D('',#30202,#24441,#24442);
#20420=AXIS2_PLACEMENT_3D('',#30208,#24446,#24447);
#20421=AXIS2_PLACEMENT_3D('',#30212,#24450,#24451);
#20422=AXIS2_PLACEMENT_3D('',#30216,#24454,#24455);
#20423=AXIS2_PLACEMENT_3D('',#30220,#24458,#24459);
#20424=AXIS2_PLACEMENT_3D('',#30224,#24462,#24463);
#20425=AXIS2_PLACEMENT_3D('',#30226,#24465,#24466);
#24398=DIRECTION('axis',(0.,0.,1.));
#24399=DIRECTION('refdir',(1.,0.,0.));
#24400=DIRECTION('center_axis',(0.,1.,0.));
#24401=DIRECTION('ref_axis',(1.,0.,0.));
#24402=DIRECTION('center_axis',(0.,1.,0.));
#24403=DIRECTION('ref_axis',(1.,0.,0.));
#24404=DIRECTION('',(0.5,0.,0.866025403784439));
#24405=DIRECTION('',(1.,0.,1.20185167898973E-16));
#24406=DIRECTION('',(0.5,0.,-0.866025403784439));
#24407=DIRECTION('',(-0.5,0.,-0.866025403784439));
#24408=DIRECTION('',(-1.,0.,-2.40370335797945E-16));
#24409=DIRECTION('',(-0.5,0.,0.866025403784439));
#24410=DIRECTION('center_axis',(0.,1.,0.));
#24411=DIRECTION('ref_axis',(0.,0.,1.));
#24412=DIRECTION('center_axis',(0.,-1.,0.));
#24413=DIRECTION('ref_axis',(1.,0.,0.));
#24414=DIRECTION('center_axis',(0.,-1.,0.));
#24415=DIRECTION('ref_axis',(1.,0.,0.));
#24416=DIRECTION('center_axis',(0.,-1.,0.));
#24417=DIRECTION('ref_axis',(1.,0.,0.));
#24418=DIRECTION('',(0.707106781186548,0.707106781186547,8.65956056235493E-17));
#24419=DIRECTION('center_axis',(0.,-1.,0.));
#24420=DIRECTION('ref_axis',(1.,0.,0.));
#24421=DIRECTION('center_axis',(0.,-1.,0.));
#24422=DIRECTION('ref_axis',(1.,0.,0.));
#24423=DIRECTION('',(0.,1.,0.));
#24424=DIRECTION('center_axis',(0.,1.,0.));
#24425=DIRECTION('ref_axis',(1.,0.,0.));
#24426=DIRECTION('center_axis',(0.,-1.,0.));
#24427=DIRECTION('ref_axis',(1.,0.,0.));
#24428=DIRECTION('',(-0.707106781186547,0.707106781186548,-8.65956056235493E-17));
#24429=DIRECTION('center_axis',(0.,-1.,0.));
#24430=DIRECTION('ref_axis',(0.,0.,-1.));
#24431=DIRECTION('center_axis',(0.,-1.,0.));
#24432=DIRECTION('ref_axis',(1.,0.,0.));
#24433=DIRECTION('center_axis',(0.,1.,0.));
#24434=DIRECTION('ref_axis',(1.,0.,0.));
#24435=DIRECTION('center_axis',(0.,1.,0.));
#24436=DIRECTION('ref_axis',(1.,0.,0.));
#24437=DIRECTION('',(-0.447213595499958,0.894427190999916,-5.47678698264203E-17));
#24438=DIRECTION('center_axis',(0.,-1.,0.));
#24439=DIRECTION('ref_axis',(1.,0.,0.));
#24440=DIRECTION('',(0.,1.,0.));
#24441=DIRECTION('center_axis',(0.866025403784439,0.,-0.5));
#24442=DIRECTION('ref_axis',(0.5,0.,0.866025403784439));
#24443=DIRECTION('',(-0.5,0.,-0.866025403784439));
#24444=DIRECTION('',(0.,-1.,0.));
#24445=DIRECTION('',(0.,-1.,0.));
#24446=DIRECTION('center_axis',(1.20185167898973E-16,0.,-1.));
#24447=DIRECTION('ref_axis',(1.,0.,1.20185167898973E-16));
#24448=DIRECTION('',(-1.,0.,-1.20185167898973E-16));
#24449=DIRECTION('',(0.,-1.,0.));
#24450=DIRECTION('center_axis',(-0.866025403784439,0.,-0.5));
#24451=DIRECTION('ref_axis',(0.5,0.,-0.866025403784439));
#24452=DIRECTION('',(-0.5,0.,0.866025403784439));
#24453=DIRECTION('',(0.,-1.,0.));
#24454=DIRECTION('center_axis',(-0.866025403784439,0.,0.5));
#24455=DIRECTION('ref_axis',(-0.5,0.,-0.866025403784439));
#24456=DIRECTION('',(0.5,0.,0.866025403784439));
#24457=DIRECTION('',(0.,-1.,0.));
#24458=DIRECTION('center_axis',(-2.40370335797945E-16,0.,1.));
#24459=DIRECTION('ref_axis',(-1.,0.,-2.40370335797945E-16));
#24460=DIRECTION('',(1.,0.,2.40370335797945E-16));
#24461=DIRECTION('',(0.,-1.,0.));
#24462=DIRECTION('center_axis',(0.866025403784439,0.,0.5));
#24463=DIRECTION('ref_axis',(-0.5,0.,0.866025403784439));
#24464=DIRECTION('',(0.5,0.,-0.866025403784439));
#24465=DIRECTION('center_axis',(0.,1.,0.));
#24466=DIRECTION('ref_axis',(1.,0.,0.));
#30162=CARTESIAN_POINT('',(0.,0.,0.));
#30163=CARTESIAN_POINT('Origin',(0.,-0.8,0.));
#30164=CARTESIAN_POINT('',(-0.24505,-0.8,3.00099698131059E-17));
#30165=CARTESIAN_POINT('Origin',(0.,-0.8,0.));
#30166=CARTESIAN_POINT('',(0.115470053837925,-0.8,-0.2));
#30167=CARTESIAN_POINT('',(0.23094010767585,-0.8,0.));
#30168=CARTESIAN_POINT('',(0.23094010767585,-0.8,0.));
#30169=CARTESIAN_POINT('',(-0.115470053837925,-0.8,-0.2));
#30170=CARTESIAN_POINT('',(0.115470053837925,-0.8,-0.2));
#30171=CARTESIAN_POINT('',(-0.23094010767585,-0.8,-2.77555756156289E-17));
#30172=CARTESIAN_POINT('',(-0.115470053837925,-0.8,-0.2));
#30173=CARTESIAN_POINT('',(-0.115470053837925,-0.8,0.2));
#30174=CARTESIAN_POINT('',(-0.23094010767585,-0.8,-2.82820063659975E-17));
#30175=CARTESIAN_POINT('',(0.115470053837925,-0.8,0.2));
#30176=CARTESIAN_POINT('',(-0.115470053837925,-0.8,0.2));
#30177=CARTESIAN_POINT('',(0.115470053837925,-0.8,0.2));
#30178=CARTESIAN_POINT('Origin',(0.375,0.5,0.));
#30179=CARTESIAN_POINT('',(-0.375,0.5,-4.59242549680257E-17));
#30180=CARTESIAN_POINT('Origin',(0.,0.5,0.));
#30181=CARTESIAN_POINT('Origin',(0.,0.475,0.));
#30182=CARTESIAN_POINT('',(-0.425,0.45,-5.20474889637625E-17));
#30183=CARTESIAN_POINT('Origin',(0.,0.45,0.));
#30184=CARTESIAN_POINT('',(-0.4,0.475,-4.89858719658941E-17));
#30185=CARTESIAN_POINT('Origin',(0.,0.24,0.));
#30186=CARTESIAN_POINT('',(-0.425,0.0299999999999998,-5.20474889637625E-17));
#30187=CARTESIAN_POINT('Origin',(0.,0.0299999999999998,0.));
#30188=CARTESIAN_POINT('',(-0.425,0.24,-5.20474889637625E-17));
#30189=CARTESIAN_POINT('Origin',(0.,0.0150000000000001,0.));
#30190=CARTESIAN_POINT('',(-0.395,4.85722573273506E-17,-4.83735485663204E-17));
#30191=CARTESIAN_POINT('Origin',(0.,0.,0.));
#30192=CARTESIAN_POINT('',(-0.41,0.0150000000000001,-5.02105187650415E-17));
#30193=CARTESIAN_POINT('Origin',(0.27,0.,0.));
#30194=CARTESIAN_POINT('',(-0.27,0.,-3.30654635769785E-17));
#30195=CARTESIAN_POINT('Origin',(0.,0.,0.));
#30196=CARTESIAN_POINT('Origin',(0.,-0.02,0.));
#30197=CARTESIAN_POINT('',(-0.24505,-0.0498999999999999,3.00099698131059E-17));
#30198=CARTESIAN_POINT('Origin',(0.,-0.0498999999999999,0.));
#30199=CARTESIAN_POINT('',(-0.26,-0.02,-3.18408167778312E-17));
#30200=CARTESIAN_POINT('Origin',(0.,-0.995,0.));
#30201=CARTESIAN_POINT('',(-0.24505,-0.995,-3.00099698131059E-17));
#30202=CARTESIAN_POINT('Origin',(0.115470053837925,-0.5,-0.2));
#30203=CARTESIAN_POINT('',(0.23094010767585,-0.5,0.));
#30204=CARTESIAN_POINT('',(0.115470053837925,-0.5,-0.2));
#30205=CARTESIAN_POINT('',(0.23094010767585,-0.5,0.));
#30206=CARTESIAN_POINT('',(0.115470053837925,-0.5,-0.2));
#30207=CARTESIAN_POINT('',(0.23094010767585,-0.5,0.));
#30208=CARTESIAN_POINT('Origin',(-0.115470053837925,-0.5,-0.2));
#30209=CARTESIAN_POINT('',(-0.115470053837925,-0.5,-0.2));
#30210=CARTESIAN_POINT('',(0.115470053837925,-0.5,-0.2));
#30211=CARTESIAN_POINT('',(-0.115470053837925,-0.5,-0.2));
#30212=CARTESIAN_POINT('Origin',(-0.23094010767585,-0.5,-2.77555756156289E-17));
#30213=CARTESIAN_POINT('',(-0.23094010767585,-0.5,-2.82820063659975E-17));
#30214=CARTESIAN_POINT('',(-0.115470053837925,-0.5,-0.2));
#30215=CARTESIAN_POINT('',(-0.23094010767585,-0.5,-2.82820063659975E-17));
#30216=CARTESIAN_POINT('Origin',(-0.115470053837925,-0.5,0.2));
#30217=CARTESIAN_POINT('',(-0.115470053837925,-0.5,0.2));
#30218=CARTESIAN_POINT('',(-0.23094010767585,-0.5,-2.82820063659975E-17));
#30219=CARTESIAN_POINT('',(-0.115470053837925,-0.5,0.2));
#30220=CARTESIAN_POINT('Origin',(0.115470053837925,-0.5,0.2));
#30221=CARTESIAN_POINT('',(0.115470053837925,-0.5,0.2));
#30222=CARTESIAN_POINT('',(-0.115470053837925,-0.5,0.2));
#30223=CARTESIAN_POINT('',(0.115470053837925,-0.5,0.2));
#30224=CARTESIAN_POINT('Origin',(0.23094010767585,-0.5,0.));
#30225=CARTESIAN_POINT('',(0.115470053837925,-0.5,0.2));
#30226=CARTESIAN_POINT('Origin',(0.,-0.5,0.));
#43428=UNCERTAINTY_MEASURE_WITH_UNIT(LENGTH_MEASURE(0.001),#43522,
'DISTANCE_ACCURACY_VALUE',
'Maximum model space distance between geometric entities at asserted c
onnectivities');
#43453=UNCERTAINTY_MEASURE_WITH_UNIT(LENGTH_MEASURE(0.001),#43522,
'DISTANCE_ACCURACY_VALUE',
'Maximum model space distance between geometric entities at asserted c
onnectivities');
#43496=(
GEOMETRIC_REPRESENTATION_CONTEXT(3)
GLOBAL_UNCERTAINTY_ASSIGNED_CONTEXT((#43428))
GLOBAL_UNIT_ASSIGNED_CONTEXT((#43522,#43524,#43525))
REPRESENTATION_CONTEXT('','3D')
);
#43521=(
GEOMETRIC_REPRESENTATION_CONTEXT(3)
GLOBAL_UNCERTAINTY_ASSIGNED_CONTEXT((#43453))
GLOBAL_UNIT_ASSIGNED_CONTEXT((#43522,#43524,#43525))
REPRESENTATION_CONTEXT('','3D')
);
#43522=(
LENGTH_UNIT()
NAMED_UNIT(*)
SI_UNIT(.CENTI.,.METRE.)
);
#43524=(
NAMED_UNIT(*)
PLANE_ANGLE_UNIT()
SI_UNIT($,.RADIAN.)
);
#43525=(
NAMED_UNIT(*)
SI_UNIT($,.STERADIAN.)
SOLID_ANGLE_UNIT()
);
#43568=SHAPE_DEFINITION_REPRESENTATION(#43645,#43836);
#43645=PRODUCT_DEFINITION_SHAPE('',$,#43904);
#43836=SHAPE_REPRESENTATION('',(#20403),#43496);
#43861=PRODUCT_DEFINITION_CONTEXT('part definition',#44064,'design');
#43904=PRODUCT_DEFINITION('M5x8 ruler screw','M5x8 ruler screw',#43971,
#43861);
#43971=PRODUCT_DEFINITION_FORMATION('',$,#44108);
#44064=APPLICATION_CONTEXT(
'Core Data for Automotive Mechanical Design Process');
#44065=PRODUCT_CONTEXT('part definition',#44064,'mechanical');
#44108=PRODUCT('M5x8 ruler screw','M5x8 ruler screw','M5x8 ruler screw',
(#44065));
#44203=COLOUR_RGB('Black',0.12,0.14,0.17);
#44204=FILL_AREA_STYLE_COLOUR('',#44203);
#44205=FILL_AREA_STYLE('',(#44204));
#44206=SURFACE_STYLE_FILL_AREA(#44205);
#44207=SURFACE_SIDE_STYLE('',(#44206));
#44208=SURFACE_STYLE_USAGE(.BOTH.,#44207);
#44209=PRESENTATION_STYLE_ASSIGNMENT((#44208));
ENDSEC;
END-ISO-10303-21;
